ISO-10303-21;
HEADER;
/* Generated by software containing ST-Developer
 * from STEP Tools, Inc. (www.steptools.com) 
 */

FILE_DESCRIPTION(
/* description */ ('PAT-072'),
/* implementation_level */ '2;1');

FILE_NAME(
/* name */ 'Metering stem gasket (3).step',
/* time_stamp */ '2026-10-29T20:11:56-07:00',
/* author */ (''),
/* organization */ (''),
/* preprocessor_version */ 'ST-DEVELOPER v20.2',
/* originating_system */ 'Autodesk Translation Framework v15.17.0.0',
/* authorisation */ '');

FILE_SCHEMA (('AUTOMOTIVE_DESIGN { 1 0 10303 214 3 1 1 }'));
ENDSEC;

DATA;
#10=MECHANICAL_DESIGN_GEOMETRIC_PRESENTATION_REPRESENTATION('',(#347),#11432);
#275=SHAPE_REPRESENTATION_RELATIONSHIP('SRR','None',#11579,#311);
#311=ADVANCED_BREP_SHAPE_REPRESENTATION('',(#383),#11410);
#347=STYLED_ITEM('',(#11833),#383);
#383=MANIFOLD_SOLID_BREP('Body1',#6082);
#482=FACE_BOUND('',#1404,.T.);
#483=FACE_BOUND('',#1406,.T.);
#651=PLANE('',#6818);
#652=PLANE('',#6819);
#949=FACE_OUTER_BOUND('',#1401,.T.);
#950=FACE_OUTER_BOUND('',#1402,.T.);
#951=FACE_OUTER_BOUND('',#1403,.T.);
#952=FACE_OUTER_BOUND('',#1405,.T.);
#1401=EDGE_LOOP('',(#4654,#4655,#4656,#4657));
#1402=EDGE_LOOP('',(#4658,#4659,#4660,#4661));
#1403=EDGE_LOOP('',(#4662));
#1404=EDGE_LOOP('',(#4663));
#1405=EDGE_LOOP('',(#4664));
#1406=EDGE_LOOP('',(#4665));
#1836=LINE('',#10190,#2255);
#1837=LINE('',#10196,#2256);
#2255=VECTOR('',#8011,0.3);
#2256=VECTOR('',#8018,0.5);
#2679=CIRCLE('',#6813,0.3);
#2680=CIRCLE('',#6814,0.3);
#2681=CIRCLE('',#6816,0.5);
#2682=CIRCLE('',#6817,0.5);
#3028=VERTEX_POINT('',#10187);
#3029=VERTEX_POINT('',#10189);
#3030=VERTEX_POINT('',#10193);
#3031=VERTEX_POINT('',#10195);
#3616=EDGE_CURVE('',#3028,#3028,#2679,.T.);
#3617=EDGE_CURVE('',#3028,#3029,#1836,.T.);
#3618=EDGE_CURVE('',#3029,#3029,#2680,.T.);
#3619=EDGE_CURVE('',#3030,#3030,#2681,.T.);
#3620=EDGE_CURVE('',#3030,#3031,#1837,.T.);
#3621=EDGE_CURVE('',#3031,#3031,#2682,.T.);
#4654=ORIENTED_EDGE('',*,*,#3616,.F.);
#4655=ORIENTED_EDGE('',*,*,#3617,.T.);
#4656=ORIENTED_EDGE('',*,*,#3618,.T.);
#4657=ORIENTED_EDGE('',*,*,#3617,.F.);
#4658=ORIENTED_EDGE('',*,*,#3619,.F.);
#4659=ORIENTED_EDGE('',*,*,#3620,.T.);
#4660=ORIENTED_EDGE('',*,*,#3621,.T.);
#4661=ORIENTED_EDGE('',*,*,#3620,.F.);
#4662=ORIENTED_EDGE('',*,*,#3619,.T.);
#4663=ORIENTED_EDGE('',*,*,#3616,.T.);
#4664=ORIENTED_EDGE('',*,*,#3621,.F.);
#4665=ORIENTED_EDGE('',*,*,#3618,.F.);
#5630=CYLINDRICAL_SURFACE('',#6812,0.3);
#5631=CYLINDRICAL_SURFACE('',#6815,0.5);
#5848=ADVANCED_FACE('',(#949),#5630,.F.);
#5849=ADVANCED_FACE('',(#950),#5631,.T.);
#5850=ADVANCED_FACE('',(#951,#482),#651,.T.);
#5851=ADVANCED_FACE('',(#952,#483),#652,.F.);
#6082=CLOSED_SHELL('',(#5848,#5849,#5850,#5851));
#6811=AXIS2_PLACEMENT_3D('',#10185,#8005,#8006);
#6812=AXIS2_PLACEMENT_3D('',#10186,#8007,#8008);
#6813=AXIS2_PLACEMENT_3D('',#10188,#8009,#8010);
#6814=AXIS2_PLACEMENT_3D('',#10191,#8012,#8013);
#6815=AXIS2_PLACEMENT_3D('',#10192,#8014,#8015);
#6816=AXIS2_PLACEMENT_3D('',#10194,#8016,#8017);
#6817=AXIS2_PLACEMENT_3D('',#10197,#8019,#8020);
#6818=AXIS2_PLACEMENT_3D('',#10198,#8021,#8022);
#6819=AXIS2_PLACEMENT_3D('',#10199,#8023,#8024);
#8005=DIRECTION('axis',(0.,0.,1.));
#8006=DIRECTION('refdir',(1.,0.,0.));
#8007=DIRECTION('center_axis',(0.,0.,1.));
#8008=DIRECTION('ref_axis',(1.,0.,0.));
#8009=DIRECTION('center_axis',(0.,0.,-1.));
#8010=DIRECTION('ref_axis',(1.,0.,0.));
#8011=DIRECTION('',(0.,0.,-1.));
#8012=DIRECTION('center_axis',(0.,0.,-1.));
#8013=DIRECTION('ref_axis',(1.,0.,0.));
#8014=DIRECTION('center_axis',(0.,0.,1.));
#8015=DIRECTION('ref_axis',(1.,0.,0.));
#8016=DIRECTION('center_axis',(0.,0.,1.));
#8017=DIRECTION('ref_axis',(1.,0.,0.));
#8018=DIRECTION('',(0.,0.,-1.));
#8019=DIRECTION('center_axis',(0.,0.,1.));
#8020=DIRECTION('ref_axis',(1.,0.,0.));
#8021=DIRECTION('center_axis',(0.,0.,1.));
#8022=DIRECTION('ref_axis',(1.,0.,0.));
#8023=DIRECTION('center_axis',(0.,0.,1.));
#8024=DIRECTION('ref_axis',(1.,0.,0.));
#10185=CARTESIAN_POINT('',(0.,0.,0.));
#10186=CARTESIAN_POINT('Origin',(3.75,1.5,6.));
#10187=CARTESIAN_POINT('',(3.45,1.5,6.1));
#10188=CARTESIAN_POINT('Origin',(3.75,1.5,6.1));
#10189=CARTESIAN_POINT('',(3.45,1.5,6.));
#10190=CARTESIAN_POINT('',(3.45,1.5,6.));
#10191=CARTESIAN_POINT('Origin',(3.75,1.5,6.));
#10192=CARTESIAN_POINT('Origin',(3.75,1.5,6.));
#10193=CARTESIAN_POINT('',(3.25,1.5,6.1));
#10194=CARTESIAN_POINT('Origin',(3.75,1.5,6.1));
#10195=CARTESIAN_POINT('',(3.25,1.5,6.));
#10196=CARTESIAN_POINT('',(3.25,1.5,6.));
#10197=CARTESIAN_POINT('Origin',(3.75,1.5,6.));
#10198=CARTESIAN_POINT('Origin',(3.75,1.5,6.1));
#10199=CARTESIAN_POINT('Origin',(3.75,1.5,6.));
#11371=UNCERTAINTY_MEASURE_WITH_UNIT(LENGTH_MEASURE(0.001),#11433,
'DISTANCE_ACCURACY_VALUE',
'Maximum model space distance between geometric entities at asserted c
onnectivities');
#11393=UNCERTAINTY_MEASURE_WITH_UNIT(LENGTH_MEASURE(0.001),#11433,
'DISTANCE_ACCURACY_VALUE',
'Maximum model space distance between geometric entities at asserted c
onnectivities');
#11410=(
GEOMETRIC_REPRESENTATION_CONTEXT(3)
GLOBAL_UNCERTAINTY_ASSIGNED_CONTEXT((#11371))
GLOBAL_UNIT_ASSIGNED_CONTEXT((#11433,#11435,#11436))
REPRESENTATION_CONTEXT('','3D')
);
#11432=(
GEOMETRIC_REPRESENTATION_CONTEXT(3)
GLOBAL_UNCERTAINTY_ASSIGNED_CONTEXT((#11393))
GLOBAL_UNIT_ASSIGNED_CONTEXT((#11433,#11435,#11436))
REPRESENTATION_CONTEXT('','3D')
);
#11433=(
LENGTH_UNIT()
NAMED_UNIT(*)
SI_UNIT(.CENTI.,.METRE.)
);
#11435=(
NAMED_UNIT(*)
PLANE_ANGLE_UNIT()
SI_UNIT($,.RADIAN.)
);
#11436=(
NAMED_UNIT(*)
SI_UNIT($,.STERADIAN.)
SOLID_ANGLE_UNIT()
);
#11453=SHAPE_DEFINITION_REPRESENTATION(#11491,#11579);
#11491=PRODUCT_DEFINITION_SHAPE('',$,#11618);
#11579=SHAPE_REPRESENTATION('',(#6811),#11410);
#11601=PRODUCT_DEFINITION_CONTEXT('part definition',#11717,'design');
#11618=PRODUCT_DEFINITION('Metering stem gasket (3)',
'Metering stem gasket (3)',#11656,#11601);
#11656=PRODUCT_DEFINITION_FORMATION('',$,#11735);
#11717=APPLICATION_CONTEXT(
'Core Data for Automotive Mechanical Design Process');
#11718=PRODUCT_CONTEXT('part definition',#11717,'mechanical');
#11735=PRODUCT('Metering stem gasket (3)','Metering stem gasket (3)',
'Metering stem gasket (3)',(#11718));
#11827=COLOUR_RGB('Off White',0.89,0.88,0.83);
#11828=FILL_AREA_STYLE_COLOUR('',#11827);
#11829=FILL_AREA_STYLE('',(#11828));
#11830=SURFACE_STYLE_FILL_AREA(#11829);
#11831=SURFACE_SIDE_STYLE('',(#11830));
#11832=SURFACE_STYLE_USAGE(.BOTH.,#11831);
#11833=PRESENTATION_STYLE_ASSIGNMENT((#11832));
ENDSEC;
END-ISO-10303-21;
